ISO-10303-21;
HEADER;
/* Generated by software containing ST-Developer
 * from STEP Tools, Inc. (www.steptools.com) 
 */

FILE_DESCRIPTION(
/* description */ (''),
/* implementation_level */ '2;1');

FILE_NAME(
/* name */ 'Main_Housing.step',
/* time_stamp */ '2026-10-23T22:28:14+06:00',
/* author */ (''),
/* organization */ (''),
/* preprocessor_version */ 'ST-DEVELOPER v20.2',
/* originating_system */ 'Autodesk Translation Framework v15.15.0.0',
/* authorisation */ '');

FILE_SCHEMA (('AUTOMOTIVE_DESIGN { 1 0 10303 214 3 1 1 }'));
ENDSEC;

DATA;
#10=MECHANICAL_DESIGN_GEOMETRIC_PRESENTATION_REPRESENTATION('',(#103),#6753);
#77=SHAPE_REPRESENTATION_RELATIONSHIP('SRR','None',#6800,#90);
#90=ADVANCED_BREP_SHAPE_REPRESENTATION('',(#116),#6740);
#103=STYLED_ITEM('',(#6900),#116);
#116=MANIFOLD_SOLID_BREP('Main_Housing',#3752);
#129=FACE_BOUND('',#548,.T.);
#130=FACE_BOUND('',#556,.T.);
#186=PLANE('',#3916);
#187=PLANE('',#3918);
#188=PLANE('',#3921);
#189=PLANE('',#3922);
#190=PLANE('',#3923);
#191=PLANE('',#3929);
#333=FACE_OUTER_BOUND('',#546,.T.);
#334=FACE_OUTER_BOUND('',#547,.T.);
#335=FACE_OUTER_BOUND('',#549,.T.);
#336=FACE_OUTER_BOUND('',#550,.T.);
#337=FACE_OUTER_BOUND('',#551,.T.);
#338=FACE_OUTER_BOUND('',#552,.T.);
#339=FACE_OUTER_BOUND('',#553,.T.);
#340=FACE_OUTER_BOUND('',#554,.T.);
#341=FACE_OUTER_BOUND('',#555,.T.);
#546=EDGE_LOOP('',(#2456,#2457,#2458,#2459,#2460,#2461,#2462,#2463));
#547=EDGE_LOOP('',(#2464));
#548=EDGE_LOOP('',(#2465));
#549=EDGE_LOOP('',(#2466,#2467,#2468,#2469,#2470,#2471));
#550=EDGE_LOOP('',(#2472,#2473,#2474,#2475));
#551=EDGE_LOOP('',(#2476,#2477,#2478,#2479));
#552=EDGE_LOOP('',(#2480,#2481,#2482,#2483));
#553=EDGE_LOOP('',(#2484,#2485,#2486,#2487));
#554=EDGE_LOOP('',(#2488,#2489,#2490,#2491,#2492,#2493,#2494,#2495));
#555=EDGE_LOOP('',(#2496));
#556=EDGE_LOOP('',(#2497));
#816=CIRCLE('',#3912,35.);
#817=CIRCLE('',#3913,35.);
#818=CIRCLE('',#3914,35.);
#819=CIRCLE('',#3915,35.);
#820=CIRCLE('',#3917,33.);
#821=CIRCLE('',#3919,40.);
#822=CIRCLE('',#3920,40.);
#823=CIRCLE('',#3924,40.);
#824=CIRCLE('',#3926,33.);
#825=CIRCLE('',#3928,40.);
#1032=LINE('',#5568,#1318);
#1033=LINE('',#5572,#1319);
#1034=LINE('',#5577,#1320);
#1035=LINE('',#5584,#1321);
#1036=LINE('',#5589,#1322);
#1037=LINE('',#5592,#1323);
#1038=LINE('',#5593,#1324);
#1039=LINE('',#5596,#1325);
#1040=LINE('',#5597,#1326);
#1041=LINE('',#5603,#1327);
#1042=LINE('',#5607,#1328);
#1318=VECTOR('',#4371,10.);
#1319=VECTOR('',#4374,35.);
#1320=VECTOR('',#4379,10.);
#1321=VECTOR('',#4388,10.);
#1322=VECTOR('',#4393,10.);
#1323=VECTOR('',#4396,10.);
#1324=VECTOR('',#4397,10.);
#1325=VECTOR('',#4400,10.);
#1326=VECTOR('',#4401,10.);
#1327=VECTOR('',#4410,33.);
#1328=VECTOR('',#4415,40.);
#1604=VERTEX_POINT('',#5566);
#1605=VERTEX_POINT('',#5567);
#1606=VERTEX_POINT('',#5569);
#1607=VERTEX_POINT('',#5571);
#1608=VERTEX_POINT('',#5574);
#1609=VERTEX_POINT('',#5576);
#1610=VERTEX_POINT('',#5580);
#1611=VERTEX_POINT('',#5583);
#1612=VERTEX_POINT('',#5585);
#1613=VERTEX_POINT('',#5587);
#1614=VERTEX_POINT('',#5591);
#1615=VERTEX_POINT('',#5595);
#1616=VERTEX_POINT('',#5601);
#1617=VERTEX_POINT('',#5605);
#1945=EDGE_CURVE('',#1604,#1605,#1032,.T.);
#1946=EDGE_CURVE('',#1606,#1604,#816,.T.);
#1947=EDGE_CURVE('',#1606,#1607,#1033,.T.);
#1948=EDGE_CURVE('',#1607,#1607,#817,.T.);
#1949=EDGE_CURVE('',#1608,#1606,#818,.T.);
#1950=EDGE_CURVE('',#1608,#1609,#1034,.T.);
#1951=EDGE_CURVE('',#1609,#1605,#819,.T.);
#1952=EDGE_CURVE('',#1610,#1610,#820,.T.);
#1953=EDGE_CURVE('',#1604,#1611,#1035,.T.);
#1954=EDGE_CURVE('',#1611,#1612,#821,.T.);
#1955=EDGE_CURVE('',#1612,#1613,#822,.T.);
#1956=EDGE_CURVE('',#1613,#1608,#1036,.T.);
#1957=EDGE_CURVE('',#1614,#1613,#1037,.T.);
#1958=EDGE_CURVE('',#1614,#1609,#1038,.T.);
#1959=EDGE_CURVE('',#1605,#1615,#1039,.T.);
#1960=EDGE_CURVE('',#1611,#1615,#1040,.T.);
#1961=EDGE_CURVE('',#1615,#1614,#823,.T.);
#1962=EDGE_CURVE('',#1616,#1616,#824,.T.);
#1963=EDGE_CURVE('',#1616,#1610,#1041,.T.);
#1964=EDGE_CURVE('',#1617,#1617,#825,.T.);
#1965=EDGE_CURVE('',#1617,#1612,#1042,.T.);
#2456=ORIENTED_EDGE('',*,*,#1945,.F.);
#2457=ORIENTED_EDGE('',*,*,#1946,.F.);
#2458=ORIENTED_EDGE('',*,*,#1947,.T.);
#2459=ORIENTED_EDGE('',*,*,#1948,.T.);
#2460=ORIENTED_EDGE('',*,*,#1947,.F.);
#2461=ORIENTED_EDGE('',*,*,#1949,.F.);
#2462=ORIENTED_EDGE('',*,*,#1950,.T.);
#2463=ORIENTED_EDGE('',*,*,#1951,.T.);
#2464=ORIENTED_EDGE('',*,*,#1948,.F.);
#2465=ORIENTED_EDGE('',*,*,#1952,.F.);
#2466=ORIENTED_EDGE('',*,*,#1949,.T.);
#2467=ORIENTED_EDGE('',*,*,#1946,.T.);
#2468=ORIENTED_EDGE('',*,*,#1953,.T.);
#2469=ORIENTED_EDGE('',*,*,#1954,.T.);
#2470=ORIENTED_EDGE('',*,*,#1955,.T.);
#2471=ORIENTED_EDGE('',*,*,#1956,.T.);
#2472=ORIENTED_EDGE('',*,*,#1956,.F.);
#2473=ORIENTED_EDGE('',*,*,#1957,.F.);
#2474=ORIENTED_EDGE('',*,*,#1958,.T.);
#2475=ORIENTED_EDGE('',*,*,#1950,.F.);
#2476=ORIENTED_EDGE('',*,*,#1953,.F.);
#2477=ORIENTED_EDGE('',*,*,#1945,.T.);
#2478=ORIENTED_EDGE('',*,*,#1959,.T.);
#2479=ORIENTED_EDGE('',*,*,#1960,.F.);
#2480=ORIENTED_EDGE('',*,*,#1961,.F.);
#2481=ORIENTED_EDGE('',*,*,#1959,.F.);
#2482=ORIENTED_EDGE('',*,*,#1951,.F.);
#2483=ORIENTED_EDGE('',*,*,#1958,.F.);
#2484=ORIENTED_EDGE('',*,*,#1962,.F.);
#2485=ORIENTED_EDGE('',*,*,#1963,.T.);
#2486=ORIENTED_EDGE('',*,*,#1952,.T.);
#2487=ORIENTED_EDGE('',*,*,#1963,.F.);
#2488=ORIENTED_EDGE('',*,*,#1964,.F.);
#2489=ORIENTED_EDGE('',*,*,#1965,.T.);
#2490=ORIENTED_EDGE('',*,*,#1954,.F.);
#2491=ORIENTED_EDGE('',*,*,#1960,.T.);
#2492=ORIENTED_EDGE('',*,*,#1961,.T.);
#2493=ORIENTED_EDGE('',*,*,#1957,.T.);
#2494=ORIENTED_EDGE('',*,*,#1955,.F.);
#2495=ORIENTED_EDGE('',*,*,#1965,.F.);
#2496=ORIENTED_EDGE('',*,*,#1964,.T.);
#2497=ORIENTED_EDGE('',*,*,#1962,.T.);
#3478=CYLINDRICAL_SURFACE('',#3911,35.);
#3479=CYLINDRICAL_SURFACE('',#3925,33.);
#3480=CYLINDRICAL_SURFACE('',#3927,40.);
#3539=ADVANCED_FACE('',(#333),#3478,.F.);
#3540=ADVANCED_FACE('',(#334,#129),#186,.F.);
#3541=ADVANCED_FACE('',(#335),#187,.F.);
#3542=ADVANCED_FACE('',(#336),#188,.F.);
#3543=ADVANCED_FACE('',(#337),#189,.F.);
#3544=ADVANCED_FACE('',(#338),#190,.F.);
#3545=ADVANCED_FACE('',(#339),#3479,.F.);
#3546=ADVANCED_FACE('',(#340),#3480,.T.);
#3547=ADVANCED_FACE('',(#341,#130),#191,.T.);
#3752=CLOSED_SHELL('',(#3539,#3540,#3541,#3542,#3543,#3544,#3545,#3546,
#3547));
#3910=AXIS2_PLACEMENT_3D('',#5564,#4367,#4368);
#3911=AXIS2_PLACEMENT_3D('',#5565,#4369,#4370);
#3912=AXIS2_PLACEMENT_3D('',#5570,#4372,#4373);
#3913=AXIS2_PLACEMENT_3D('',#5573,#4375,#4376);
#3914=AXIS2_PLACEMENT_3D('',#5575,#4377,#4378);
#3915=AXIS2_PLACEMENT_3D('',#5578,#4380,#4381);
#3916=AXIS2_PLACEMENT_3D('',#5579,#4382,#4383);
#3917=AXIS2_PLACEMENT_3D('',#5581,#4384,#4385);
#3918=AXIS2_PLACEMENT_3D('',#5582,#4386,#4387);
#3919=AXIS2_PLACEMENT_3D('',#5586,#4389,#4390);
#3920=AXIS2_PLACEMENT_3D('',#5588,#4391,#4392);
#3921=AXIS2_PLACEMENT_3D('',#5590,#4394,#4395);
#3922=AXIS2_PLACEMENT_3D('',#5594,#4398,#4399);
#3923=AXIS2_PLACEMENT_3D('',#5598,#4402,#4403);
#3924=AXIS2_PLACEMENT_3D('',#5599,#4404,#4405);
#3925=AXIS2_PLACEMENT_3D('',#5600,#4406,#4407);
#3926=AXIS2_PLACEMENT_3D('',#5602,#4408,#4409);
#3927=AXIS2_PLACEMENT_3D('',#5604,#4411,#4412);
#3928=AXIS2_PLACEMENT_3D('',#5606,#4413,#4414);
#3929=AXIS2_PLACEMENT_3D('',#5608,#4416,#4417);
#4367=DIRECTION('axis',(0.,0.,1.));
#4368=DIRECTION('refdir',(1.,0.,0.));
#4369=DIRECTION('center_axis',(0.,1.,0.));
#4370=DIRECTION('ref_axis',(1.,0.,0.));
#4371=DIRECTION('',(0.,1.,0.));
#4372=DIRECTION('center_axis',(0.,1.,0.));
#4373=DIRECTION('ref_axis',(1.,0.,0.));
#4374=DIRECTION('',(0.,1.,0.));
#4375=DIRECTION('center_axis',(0.,1.,0.));
#4376=DIRECTION('ref_axis',(1.,0.,0.));
#4377=DIRECTION('center_axis',(0.,1.,0.));
#4378=DIRECTION('ref_axis',(1.,0.,0.));
#4379=DIRECTION('',(0.,1.,0.));
#4380=DIRECTION('center_axis',(0.,-1.,0.));
#4381=DIRECTION('ref_axis',(1.,0.,0.));
#4382=DIRECTION('center_axis',(0.,1.,0.));
#4383=DIRECTION('ref_axis',(1.,0.,0.));
#4384=DIRECTION('center_axis',(0.,-1.,0.));
#4385=DIRECTION('ref_axis',(1.,0.,0.));
#4386=DIRECTION('center_axis',(0.,1.,0.));
#4387=DIRECTION('ref_axis',(1.,0.,0.));
#4388=DIRECTION('',(-0.795671922146114,0.,0.605727820318918));
#4389=DIRECTION('center_axis',(0.,-1.,0.));
#4390=DIRECTION('ref_axis',(1.,0.,0.));
#4391=DIRECTION('center_axis',(0.,-1.,0.));
#4392=DIRECTION('ref_axis',(1.,0.,0.));
#4393=DIRECTION('',(-0.795671922146114,0.,-0.605727820318918));
#4394=DIRECTION('center_axis',(0.605727820318918,0.,-0.795671922146114));
#4395=DIRECTION('ref_axis',(-0.795671922146114,0.,-0.605727820318918));
#4396=DIRECTION('',(0.,-1.,0.));
#4397=DIRECTION('',(-0.795671922146114,0.,-0.605727820318918));
#4398=DIRECTION('center_axis',(-0.605727820318918,0.,-0.795671922146114));
#4399=DIRECTION('ref_axis',(-0.795671922146114,0.,0.605727820318918));
#4400=DIRECTION('',(-0.795671922146114,0.,0.605727820318918));
#4401=DIRECTION('',(0.,1.,0.));
#4402=DIRECTION('center_axis',(0.,1.,0.));
#4403=DIRECTION('ref_axis',(1.,0.,0.));
#4404=DIRECTION('center_axis',(0.,1.,0.));
#4405=DIRECTION('ref_axis',(1.,0.,0.));
#4406=DIRECTION('center_axis',(0.,1.,0.));
#4407=DIRECTION('ref_axis',(1.,0.,0.));
#4408=DIRECTION('center_axis',(0.,-1.,0.));
#4409=DIRECTION('ref_axis',(1.,0.,0.));
#4410=DIRECTION('',(0.,-1.,0.));
#4411=DIRECTION('center_axis',(0.,1.,0.));
#4412=DIRECTION('ref_axis',(1.,0.,0.));
#4413=DIRECTION('center_axis',(0.,1.,0.));
#4414=DIRECTION('ref_axis',(1.,0.,0.));
#4415=DIRECTION('',(0.,-1.,0.));
#4416=DIRECTION('center_axis',(0.,1.,0.));
#4417=DIRECTION('ref_axis',(1.,0.,0.));
#5564=CARTESIAN_POINT('',(0.,0.,0.));
#5565=CARTESIAN_POINT('Origin',(0.,0.,114.33240815703));
#5566=CARTESIAN_POINT('',(-27.848517275114,-4.,135.532881868193));
#5567=CARTESIAN_POINT('',(-27.848517275114,2.,135.532881868193));
#5568=CARTESIAN_POINT('',(-27.848517275114,0.,135.532881868193));
#5569=CARTESIAN_POINT('',(-35.,-4.,114.33240815703));
#5570=CARTESIAN_POINT('Origin',(0.,-4.,114.33240815703));
#5571=CARTESIAN_POINT('',(-35.,3.,114.33240815703));
#5572=CARTESIAN_POINT('',(-35.,0.,114.33240815703));
#5573=CARTESIAN_POINT('Origin',(0.,3.,114.33240815703));
#5574=CARTESIAN_POINT('',(27.848517275114,-4.,135.532881868193));
#5575=CARTESIAN_POINT('Origin',(0.,-4.,114.33240815703));
#5576=CARTESIAN_POINT('',(27.848517275114,2.,135.532881868193));
#5577=CARTESIAN_POINT('',(27.848517275114,0.,135.532881868193));
#5578=CARTESIAN_POINT('Origin',(0.,2.,114.33240815703));
#5579=CARTESIAN_POINT('Origin',(0.,3.,114.33240815703));
#5580=CARTESIAN_POINT('',(-33.,3.,114.33240815703));
#5581=CARTESIAN_POINT('Origin',(0.,3.,114.33240815703));
#5582=CARTESIAN_POINT('Origin',(0.,-4.,114.33240815703));
#5583=CARTESIAN_POINT('',(-31.8268768858446,-4.,138.561520969787));
#5584=CARTESIAN_POINT('',(-13.924258637557,-4.,124.932645012611));
#5585=CARTESIAN_POINT('',(-40.,-4.,114.33240815703));
#5586=CARTESIAN_POINT('Origin',(0.,-4.,114.33240815703));
#5587=CARTESIAN_POINT('',(31.8268768858446,-4.,138.561520969787));
#5588=CARTESIAN_POINT('Origin',(0.,-4.,114.33240815703));
#5589=CARTESIAN_POINT('',(15.9134384429223,-4.,126.446964563409));
#5590=CARTESIAN_POINT('Origin',(31.8268768858446,0.,138.561520969787));
#5591=CARTESIAN_POINT('',(31.8268768858446,2.,138.561520969787));
#5592=CARTESIAN_POINT('',(31.8268768858446,0.,138.561520969787));
#5593=CARTESIAN_POINT('',(31.8268768858446,2.,138.561520969787));
#5594=CARTESIAN_POINT('Origin',(-27.848517275114,0.,135.532881868193));
#5595=CARTESIAN_POINT('',(-31.8268768858446,2.,138.561520969787));
#5596=CARTESIAN_POINT('',(-31.8268768858446,2.,138.561520969787));
#5597=CARTESIAN_POINT('',(-31.8268768858446,0.,138.561520969787));
#5598=CARTESIAN_POINT('Origin',(0.,2.,144.932645012611));
#5599=CARTESIAN_POINT('Origin',(0.,2.,114.33240815703));
#5600=CARTESIAN_POINT('Origin',(0.,0.,114.33240815703));
#5601=CARTESIAN_POINT('',(-33.,4.,114.33240815703));
#5602=CARTESIAN_POINT('Origin',(0.,4.,114.33240815703));
#5603=CARTESIAN_POINT('',(-33.,0.,114.33240815703));
#5604=CARTESIAN_POINT('Origin',(0.,0.,114.33240815703));
#5605=CARTESIAN_POINT('',(-40.,4.,114.33240815703));
#5606=CARTESIAN_POINT('Origin',(0.,4.,114.33240815703));
#5607=CARTESIAN_POINT('',(-40.,0.,114.33240815703));
#5608=CARTESIAN_POINT('Origin',(0.,4.,114.33240815703));
#6725=UNCERTAINTY_MEASURE_WITH_UNIT(LENGTH_MEASURE(0.01),#6754,
'DISTANCE_ACCURACY_VALUE',
'Maximum model space distance between geometric entities at asserted c
onnectivities');
#6738=UNCERTAINTY_MEASURE_WITH_UNIT(LENGTH_MEASURE(0.01),#6754,
'DISTANCE_ACCURACY_VALUE',
'Maximum model space distance between geometric entities at asserted c
onnectivities');
#6740=(
GEOMETRIC_REPRESENTATION_CONTEXT(3)
GLOBAL_UNCERTAINTY_ASSIGNED_CONTEXT((#6725))
GLOBAL_UNIT_ASSIGNED_CONTEXT((#6754,#6756,#6757))
REPRESENTATION_CONTEXT('','3D')
);
#6753=(
GEOMETRIC_REPRESENTATION_CONTEXT(3)
GLOBAL_UNCERTAINTY_ASSIGNED_CONTEXT((#6738))
GLOBAL_UNIT_ASSIGNED_CONTEXT((#6754,#6756,#6757))
REPRESENTATION_CONTEXT('','3D')
);
#6754=(
LENGTH_UNIT()
NAMED_UNIT(*)
SI_UNIT(.MILLI.,.METRE.)
);
#6756=(
NAMED_UNIT(*)
PLANE_ANGLE_UNIT()
SI_UNIT($,.RADIAN.)
);
#6757=(
NAMED_UNIT(*)
SI_UNIT($,.STERADIAN.)
SOLID_ANGLE_UNIT()
);
#6759=SHAPE_DEFINITION_REPRESENTATION(#6773,#6800);
#6773=PRODUCT_DEFINITION_SHAPE('',$,#6815);
#6800=SHAPE_REPRESENTATION('',(#3910),#6740);
#6813=PRODUCT_DEFINITION_CONTEXT('part definition',#6857,'design');
#6815=PRODUCT_DEFINITION('Main_Housing','Main_Housing',#6829,#6813);
#6829=PRODUCT_DEFINITION_FORMATION('',$,#6860);
#6857=APPLICATION_CONTEXT(
'Core Data for Automotive Mechanical Design Process');
#6858=PRODUCT_CONTEXT('part definition',#6857,'mechanical');
#6860=PRODUCT('Main_Housing','Main_Housing',$,(#6858));
#6894=COLOUR_RGB('Dark Blue',0.08,0.2,0.34);
#6895=FILL_AREA_STYLE_COLOUR('',#6894);
#6896=FILL_AREA_STYLE('',(#6895));
#6897=SURFACE_STYLE_FILL_AREA(#6896);
#6898=SURFACE_SIDE_STYLE('',(#6897));
#6899=SURFACE_STYLE_USAGE(.BOTH.,#6898);
#6900=PRESENTATION_STYLE_ASSIGNMENT((#6899));
ENDSEC;
END-ISO-10303-21;
